ISO-10303-21;
HEADER;
FILE_DESCRIPTION (('STEP AP214'),
    '1' );
FILE_NAME ('socket head cap screw_iso_ISO 4762 M5 x 8 - 8N.step',
    '2026-10-04T13:31:42',
    ( '' ),
    ( '' ),
    'SwSTEP 2.0',
    'SolidWorks 2026',
    '' );
FILE_SCHEMA (( 'AUTOMOTIVE_DESIGN' ));
ENDSEC;

DATA;
#360=CARTESIAN_POINT ( 'NONE',  ( 0.2500000000000002220, 0.000000000000000000, 0.000000000000000000 ) ) ;
#482=EDGE_CURVE ( 'NONE', #89587, #45951, #50207, .T. ) ;
#947=LINE ( 'NONE', #122312, #12055 ) ;
#1370=PLANE ( 'NONE',  #27795 ) ;
#1729=CARTESIAN_POINT ( 'NONE',  ( -31.74999999999995737, 0.000000000000000000, 0.000000000000000000 ) ) ;
#2269=EDGE_LOOP ( 'NONE', ( #119206, #10771, #58766, #37881 ) ) ;
#2452=CIRCLE ( 'NONE', #137990, 2.500000000000000444 ) ;
#2768=ADVANCED_FACE ( 'NONE', ( #20375 ), #134223, .F. ) ;
#2933=CARTESIAN_POINT ( 'NONE',  ( 2.500000000000000000, 1.178949249685212974, -2.042000000000001148 ) ) ;
#3142=AXIS2_PLACEMENT_3D ( 'NONE', #21155, #119173, #40320 ) ;
#4122=ADVANCED_FACE ( 'NONE', ( #197229 ), #62878, .F. ) ;
#4163=VERTEX_POINT ( 'NONE', #90027 ) ;
#4761=SHAPE_DEFINITION_REPRESENTATION ( #137256, #9542 ) ;
#4797=FACE_OUTER_BOUND ( 'NONE', #30547, .T. ) ;
#4904=DIRECTION ( 'NONE',  ( 0.000000000000000000, -1.000000000000000000, 1.287488025362403787E-15 ) ) ;
#5002=LINE ( 'NONE', #17212, #21917 ) ;
#5156=ORIENTED_EDGE ( 'NONE', *, *, #165915, .T. ) ;
#5268=ORIENTED_EDGE ( 'NONE', *, *, #8681, .F. ) ;
#5450=UNCERTAINTY_MEASURE_WITH_UNIT (LENGTH_MEASURE( 1.000000000000000082E-05 ), #162691, 'distance_accuracy_value', 'NONE');
#5649=ORIENTED_EDGE ( 'NONE', *, *, #90472, .F. ) ;
#5884=PRODUCT_DEFINITION_CONTEXT ( 'detailed design', #143659, 'design' ) ;
#5939=CARTESIAN_POINT ( 'NONE',  ( 2.500000000000000000, -1.178949249685214307, 2.042000000000002036 ) ) ;
#5950=DIRECTION ( 'NONE',  ( 0.000000000000000000, -0.5000000000000011102, -0.8660254037844379305 ) ) ;
#6190=DIRECTION ( 'NONE',  ( 0.000000000000000000, 0.000000000000000000, -1.000000000000000000 ) ) ;
#6226=EDGE_LOOP ( 'NONE', ( #121374, #45710 ) ) ;
#6505=ORIENTED_EDGE ( 'NONE', *, *, #136550, .T. ) ;
#6747=CARTESIAN_POINT ( 'NONE',  ( 2.500000000000000000, -1.178949249685214307, 2.042000000000002036 ) ) ;
#6911=DIRECTION ( 'NONE',  ( 0.000000000000000000, 0.4999999999999993894, -0.8660254037844389297 ) ) ;
#6990=PLANE ( 'NONE',  #143579 ) ;
#7157=VERTEX_POINT ( 'NONE', #106535 ) ;
#7196=DIRECTION ( 'NONE',  ( -1.000000000000000000, -0.000000000000000000, -0.000000000000000000 ) ) ;
#7520=EDGE_CURVE ( 'NONE', #167413, #66922, #31693, .T. ) ;
#8218=DIRECTION ( 'NONE',  ( 0.000000000000000000, -1.224646799147353454E-16, 1.000000000000000000 ) ) ;
#8238=VERTEX_POINT ( 'NONE', #130153 ) ;
#8681=EDGE_CURVE ( 'NONE', #167085, #7157, #101715, .T. ) ;
#8778=DIRECTION ( 'NONE',  ( 0.000000000000000000, 1.000000000000000000, -1.471414886128461669E-15 ) ) ;
#8968=CARTESIAN_POINT ( 'NONE',  ( 2.500000000000000000, -1.178949249685214307, 2.042000000000002036 ) ) ;
#9231=DIRECTION ( 'NONE',  ( 0.000000000000000000, 0.000000000000000000, 1.000000000000000000 ) ) ;
#9419=ORIENTED_EDGE ( 'NONE', *, *, #92161, .F. ) ;
#9447=CARTESIAN_POINT ( 'NONE',  ( 12.99999999999999822, 0.000000000000000000, 0.000000000000000000 ) ) ;
#9542=SHAPE_REPRESENTATION ( 'socket head cap screw_iso_ISO 4762 M5 x 8 - 8N', ( #82054 ), #85555 ) ;
#9951=ORIENTED_EDGE ( 'NONE', *, *, #182035, .F. ) ;
#10420=VERTEX_POINT ( 'NONE', #81182 ) ;
#10475=EDGE_CURVE ( 'NONE', #137833, #171158, #174224, .T. ) ;
#10620=DIRECTION ( 'NONE',  ( 1.000000000000000000, 0.000000000000000000, 0.000000000000000000 ) ) ;
#10662=ORIENTED_EDGE ( 'NONE', *, *, #153660, .F. ) ;
#10771=ORIENTED_EDGE ( 'NONE', *, *, #182212, .T. ) ;
#11050=AXIS2_PLACEMENT_3D ( 'NONE', #86392, #179429, #71233 ) ;
#11471=DIRECTION ( 'NONE',  ( 0.000000000000000000, 0.000000000000000000, 1.000000000000000000 ) ) ;
#11536=EDGE_CURVE ( 'NONE', #80788, #101588, #114695, .T. ) ;
#11768=MANIFOLD_SOLID_BREP ( 'Hex', #111522 ) ;
#11869=CIRCLE ( 'NONE', #124829, 2.041999999999999815 ) ;
#12024=PLANE ( 'NONE',  #47024 ) ;
#12055=VECTOR ( 'NONE', #187988, 1000.000000000000114 ) ;
#12884=EDGE_LOOP ( 'NONE', ( #97241, #180583, #38933, #34189 ) ) ;
#13716=ORIENTED_EDGE ( 'NONE', *, *, #175617, .T. ) ;
#13980=AXIS2_PLACEMENT_3D ( 'NONE', #187769, #127049, #142226 ) ;
#14106=ADVANCED_FACE ( 'NONE', ( #101685 ), #83507, .T. ) ;
#14532=CARTESIAN_POINT ( 'NONE',  ( 2.500000000000000000, 1.178949249685217193, 2.041999999999998483 ) ) ;
#15409=DIRECTION ( 'NONE',  ( 0.000000000000000000, 0.000000000000000000, 1.000000000000000000 ) ) ;
#15884=DIRECTION ( 'NONE',  ( -0.000000000000000000, 0.000000000000000000, 1.000000000000000000 ) ) ;
#15936=FACE_OUTER_BOUND ( 'NONE', #169670, .T. ) ;
#15966=EDGE_LOOP ( 'NONE', ( #135007, #65086, #24148, #59142 ) ) ;
#16052=EDGE_CURVE ( 'NONE', #76856, #89587, #83270, .T. ) ;
#16173=CARTESIAN_POINT ( 'NONE',  ( 5.199999999999996625, 0.000000000000000000, 0.000000000000000000 ) ) ;
#16321=SURFACE_STYLE_FILL_AREA ( #31486 ) ;
#16610=VERTEX_POINT ( 'NONE', #144944 ) ;
#16770=AXIS2_PLACEMENT_3D ( 'NONE', #25477, #58765, #181147 ) ;
#17212=CARTESIAN_POINT ( 'NONE',  ( 2.500000000000000000, 2.357898499370431722, -2.818925648462311528E-15 ) ) ;
#17771=ADVANCED_FACE ( 'NONE', ( #155906 ), #106417, .F. ) ;
#17985=ORIENTED_EDGE ( 'NONE', *, *, #75323, .F. ) ;
#18326=VECTOR ( 'NONE', #124731, 1000.000000000000000 ) ;
#18400=CARTESIAN_POINT ( 'NONE',  ( 0.2500000000000002220, 0.000000000000000000, 0.000000000000000000 ) ) ;
#18410=DIRECTION ( 'NONE',  ( -0.000000000000000000, 1.471414886128461471E-15, 1.000000000000000000 ) ) ;
#18733=ADVANCED_FACE ( 'NONE', ( #135557 ), #195238, .F. ) ;
#19652=CARTESIAN_POINT ( 'NONE',  ( 2.500000000000000000, 1.178949249685212974, -2.042000000000001148 ) ) ;
#20375=FACE_OUTER_BOUND ( 'NONE', #125535, .T. ) ;
#20390=VECTOR ( 'NONE', #105550, 1000.000000000000000 ) ;
#20439=ORIENTED_EDGE ( 'NONE', *, *, #173336, .F. ) ;
#20622=ADVANCED_FACE ( 'NONE', ( #74631 ), #158162, .T. ) ;
#21155=CARTESIAN_POINT ( 'NONE',  ( 4.999999999999999112, 4.250000000000000000, 0.000000000000000000 ) ) ;
#21372=DIRECTION ( 'NONE',  ( -1.000000000000000000, -0.000000000000000000, -0.000000000000000000 ) ) ;
#21569=ORIENTED_EDGE ( 'NONE', *, *, #7520, .T. ) ;
#21917=VECTOR ( 'NONE', #49537, 999.9999999999997726 ) ;
#21946=AXIS2_PLACEMENT_3D ( 'NONE', #139266, #63424, #47272 ) ;
#22020=CARTESIAN_POINT ( 'NONE',  ( 2.500000000000000000, -2.357898499370432610, 3.252606517456513302E-15 ) ) ;
#22062=DIRECTION ( 'NONE',  ( 0.000000000000000000, -0.4999999999999993894, 0.8660254037844389297 ) ) ;
#22086=DIRECTION ( 'NONE',  ( 0.000000000000000000, 1.000000000000000000, -1.224646799147353207E-16 ) ) ;
#22134=ADVANCED_FACE ( 'NONE', ( #151512 ), #12024, .T. ) ;
#22504=CARTESIAN_POINT ( 'NONE',  ( 2.500000000000000000, 2.357898499370431722, -2.818925648462311528E-15 ) ) ;
#22603=VECTOR ( 'NONE', #78540, 1000.000000000000114 ) ;
#22778=CARTESIAN_POINT ( 'NONE',  ( 12.99999999999999822, 0.000000000000000000, 2.055000000000000160 ) ) ;
#22885=CARTESIAN_POINT ( 'NONE',  ( 2.500000000000000000, 0.000000000000000000, 0.000000000000000000 ) ) ;
#22986=ADVANCED_BREP_SHAPE_REPRESENTATION ( '', ( #11768, #82054 ), #85555 ) ;
#23413=ORIENTED_EDGE ( 'NONE', *, *, #182035, .T. ) ;
#23489=ORIENTED_EDGE ( 'NONE', *, *, #168230, .T. ) ;
#23510=EDGE_CURVE ( 'NONE', #101588, #4163, #39723, .T. ) ;
#23578=ORIENTED_EDGE ( 'NONE', *, *, #173336, .T. ) ;
#24148=ORIENTED_EDGE ( 'NONE', *, *, #198087, .F. ) ;
#24675=ORIENTED_EDGE ( 'NONE', *, *, #182212, .F. ) ;
#25477=CARTESIAN_POINT ( 'NONE',  ( 2.500000000000000000, 2.357898499370431722, -2.818925648462311528E-15 ) ) ;
#25683=ADVANCED_FACE ( 'NONE', ( #127621 ), #118468, .F. ) ;
#26201=ORIENTED_EDGE ( 'NONE', *, *, #108101, .F. ) ;
#26498=DIRECTION ( 'NONE',  ( 0.000000000000000000, 0.000000000000000000, 1.000000000000000000 ) ) ;
#26587=VERTEX_POINT ( 'NONE', #153758 ) ;
#27230=CYLINDRICAL_SURFACE ( 'NONE', #169200, 2.500000000000000444 ) ;
#27390=DIRECTION ( 'NONE',  ( 0.000000000000000000, 0.000000000000000000, -1.000000000000000000 ) ) ;
#27428=MECHANICAL_DESIGN_GEOMETRIC_PRESENTATION_REPRESENTATION('',(#79052),#111386);
#27569=AXIS2_PLACEMENT_3D ( 'NONE', #47660, #140643, #199350 ) ;
#27795=AXIS2_PLACEMENT_3D ( 'NONE', #188401, #187423, #48891 ) ;
#27878=CARTESIAN_POINT ( 'NONE',  ( 0.000000000000000000, -1.178949249685214307, 2.042000000000002036 ) ) ;
#28376=ORIENTED_EDGE ( 'NONE', *, *, #181949, .F. ) ;
#28387=CARTESIAN_POINT ( 'NONE',  ( 2.500000000000000000, -1.178949249685214307, 2.042000000000002036 ) ) ;
#28402=CARTESIAN_POINT ( 'NONE',  ( 12.55500000000001748, 0.000000000000000000, 0.000000000000000000 ) ) ;
#28412=EDGE_LOOP ( 'NONE', ( #68441, #200151, #170272 ) ) ;
#28735=DIRECTION ( 'NONE',  ( -1.000000000000000000, -0.000000000000000000, -0.000000000000000000 ) ) ;
#28856=CARTESIAN_POINT ( 'NONE',  ( -31.74999999999995737, 0.000000000000000000, 0.000000000000000000 ) ) ;
#28864=LINE ( 'NONE', #76325, #174296 ) ;
#28933=DIRECTION ( 'NONE',  ( 0.000000000000000000, 0.000000000000000000, -1.000000000000000000 ) ) ;
#29215=CARTESIAN_POINT ( 'NONE',  ( 12.99999999999999822, 0.000000000000000000, 0.000000000000000000 ) ) ;
#29588=DIRECTION ( 'NONE',  ( -1.000000000000000000, -0.000000000000000000, -0.000000000000000000 ) ) ;
#30149=VECTOR ( 'NONE', #51221, 1000.000000000000000 ) ;
#30288=DIRECTION ( 'NONE',  ( 0.000000000000000000, 0.000000000000000000, -1.000000000000000000 ) ) ;
#30441=EDGE_CURVE ( 'NONE', #193525, #80788, #75931, .T. ) ;
#30547=EDGE_LOOP ( 'NONE', ( #174696, #51288, #88771 ) ) ;
#30692=AXIS2_PLACEMENT_3D ( 'NONE', #160382, #158386, #112871 ) ;
#31152=CARTESIAN_POINT ( 'NONE',  ( 2.500000000000000000, 2.357898499370431722, -2.818925648462311528E-15 ) ) ;
#31166=ORIENTED_EDGE ( 'NONE', *, *, #95942, .T. ) ;
#31289=CARTESIAN_POINT ( 'NONE',  ( 2.500000000000000000, 0.000000000000000000, 0.000000000000000000 ) ) ;
#31486=FILL_AREA_STYLE ('',( #46656 ) ) ;
#31693=LINE ( 'NONE', #14532, #114545 ) ;
#31839=ORIENTED_EDGE ( 'NONE', *, *, #87024, .F. ) ;
#31897=CARTESIAN_POINT ( 'NONE',  ( 5.199999999999996625, 0.000000000000000000, 0.000000000000000000 ) ) ;
#32844=DIRECTION ( 'NONE',  ( 0.000000000000000000, 0.000000000000000000, 1.000000000000000000 ) ) ;
#33556=DIRECTION ( 'NONE',  ( 0.000000000000000000, 0.4999999999999991118, -0.8660254037844391517 ) ) ;
#34189=ORIENTED_EDGE ( 'NONE', *, *, #90472, .T. ) ;
#34274=LINE ( 'NONE', #2933, #150416 ) ;
#34640=AXIS2_PLACEMENT_3D ( 'NONE', #128532, #21372, #6190 ) ;
#36163=DIRECTION ( 'NONE',  ( 0.000000000000000000, 0.000000000000000000, -1.000000000000000000 ) ) ;
#36888=AXIS2_PLACEMENT_3D ( 'NONE', #52183, #146182, #100678 ) ;
#37032=EDGE_CURVE ( 'NONE', #137833, #66922, #192917, .T. ) ;
#37547=VECTOR ( 'NONE', #174337, 1000.000000000000000 ) ;
#37881=ORIENTED_EDGE ( 'NONE', *, *, #95942, .F. ) ;
#38345=FACE_OUTER_BOUND ( 'NONE', #107153, .T. ) ;
#38560=VERTEX_POINT ( 'NONE', #139102 ) ;
#38933=ORIENTED_EDGE ( 'NONE', *, *, #190368, .T. ) ;
#39296=LINE ( 'NONE', #144465, #79954 ) ;
#39723=CIRCLE ( 'NONE', #165742, 2.041999999999999815 ) ;
#39751=AXIS2_PLACEMENT_3D ( 'NONE', #174676, #128149, #97793 ) ;
#39764=CARTESIAN_POINT ( 'NONE',  ( 2.500000000000000000, 2.500728763858895382E-16, -2.041999999999999815 ) ) ;
#39916=CARTESIAN_POINT ( 'NONE',  ( 2.500000000000000000, -2.629050547790028551E-15, -2.041999999999999815 ) ) ;
#40205=AXIS2_PLACEMENT_3D ( 'NONE', #31289, #167818, #168790 ) ;
#40320=DIRECTION ( 'NONE',  ( 0.000000000000000000, 0.000000000000000000, -1.000000000000000000 ) ) ;
#41053=VERTEX_POINT ( 'NONE', #193713 ) ;
#41289=DIRECTION ( 'NONE',  ( -0.7071067811865312525, 0.000000000000000000, 0.7071067811865637820 ) ) ;
#41538=ADVANCED_FACE ( 'NONE', ( #87516 ), #196719, .T. ) ;
#42433=CARTESIAN_POINT ( 'NONE',  ( 0.000000000000000000, 1.178949249685212974, -2.042000000000001148 ) ) ;
#42779=LINE ( 'NONE', #39764, #124679 ) ;
#43675=DIRECTION ( 'NONE',  ( 0.000000000000000000, 0.000000000000000000, 1.000000000000000000 ) ) ;
#44177=AXIS2_PLACEMENT_3D ( 'NONE', #125969, #175460, #141135 ) ;
#44323=VECTOR ( 'NONE', #104912, 1000.000000000000114 ) ;
#45230=CARTESIAN_POINT ( 'NONE',  ( 4.999999999999997335, 3.306546357697854226E-16, 2.700000000000000622 ) ) ;
#45710=ORIENTED_EDGE ( 'NONE', *, *, #74806, .T. ) ;
#45951=VERTEX_POINT ( 'NONE', #92400 ) ;
#46474=DIRECTION ( 'NONE',  ( -1.000000000000000000, -0.000000000000000000, -0.000000000000000000 ) ) ;
#46656=FILL_AREA_STYLE_COLOUR ( '', #79181 ) ;
#47024=AXIS2_PLACEMENT_3D ( 'NONE', #59478, #89832, #73686 ) ;
#47272=DIRECTION ( 'NONE',  ( 0.000000000000000000, 0.5000000000000011102, 0.8660254037844379305 ) ) ;
#47660=CARTESIAN_POINT ( 'NONE',  ( 2.500000000000000000, 0.000000000000000000, 0.000000000000000000 ) ) ;
#47905=CARTESIAN_POINT ( 'NONE',  ( -31.74999999999995737, 5.204748896376250699E-16, -4.250000000000000000 ) ) ;
#48891=DIRECTION ( 'NONE',  ( 0.000000000000000000, 1.000000000000000000, -1.287488025362403787E-15 ) ) ;
#49298=LINE ( 'NONE', #31152, #101611 ) ;
#49489=ADVANCED_FACE ( 'NONE', ( #38345 ), #6990, .F. ) ;
#49537=DIRECTION ( 'NONE',  ( 0.000000000000000000, -0.5000000000000013323, -0.8660254037844380415 ) ) ;
#49638=PRESENTATION_STYLE_ASSIGNMENT (( #139638 ) ) ;
#49752=AXIS2_PLACEMENT_3D ( 'NONE', #117386, #7196, #130540 ) ;
#49922=VERTEX_POINT ( 'NONE', #126134 ) ;
#50044=EDGE_CURVE ( 'NONE', #100590, #137833, #49298, .T. ) ;
#50207=CIRCLE ( 'NONE', #143405, 2.041999999999999815 ) ;
#50745=ORIENTED_EDGE ( 'NONE', *, *, #107988, .T. ) ;
#51040=CARTESIAN_POINT ( 'NONE',  ( 2.500000000000000000, -1.178949249685218970, -2.041999999999998039 ) ) ;
#51221=DIRECTION ( 'NONE',  ( -1.000000000000000000, -0.000000000000000000, -0.000000000000000000 ) ) ;
#51288=ORIENTED_EDGE ( 'NONE', *, *, #16052, .T. ) ;
#51342=ORIENTED_EDGE ( 'NONE', *, *, #113885, .T. ) ;
#51469=CARTESIAN_POINT ( 'NONE',  ( 2.500000000000000000, 1.178949249685212974, -2.042000000000001148 ) ) ;
#51496=FACE_OUTER_BOUND ( 'NONE', #76820, .T. ) ;
#51827=AXIS2_PLACEMENT_3D ( 'NONE', #28856, #58188, #149204 ) ;
#51857=CARTESIAN_POINT ( 'NONE',  ( 0.000000000000000000, 2.357898499370431722, -2.818925648462311528E-15 ) ) ;
#52028=LINE ( 'NONE', #51040, #82952 ) ;
#52086=CARTESIAN_POINT ( 'NONE',  ( 0.000000000000000000, -2.357898499370432610, 3.252606517456513302E-15 ) ) ;
#52183=CARTESIAN_POINT ( 'NONE',  ( 13.00000000000000000, 2.055000000000000160, 0.000000000000000000 ) ) ;
#52984=EDGE_LOOP ( 'NONE', ( #51342, #10662, #149771 ) ) ;
#53446=CARTESIAN_POINT ( 'NONE',  ( 12.99999999999999822, 0.000000000000000000, 2.055000000000000160 ) ) ;
#53532=AXIS2_PLACEMENT_3D ( 'NONE', #9447, #29588, #189000 ) ;
#54143=CIRCLE ( 'NONE', #34640, 2.700000000000000622 ) ;
#55063=CARTESIAN_POINT ( 'NONE',  ( 2.500000000000000000, -1.178949249685214307, 2.042000000000002036 ) ) ;
#55108=CARTESIAN_POINT ( 'NONE',  ( 0.000000000000000000, 0.000000000000000000, 0.000000000000000000 ) ) ;
#56135=CIRCLE ( 'NONE', #98071, 2.500000000000000444 ) ;
#56314=ADVANCED_FACE ( 'NONE', ( #85792 ), #147478, .F. ) ;
#56520=FILL_AREA_STYLE_COLOUR ( '', #169409 ) ;
#56559=DIRECTION ( 'NONE',  ( -1.000000000000000000, -0.000000000000000000, -0.000000000000000000 ) ) ;
#56564=AXIS2_PLACEMENT_3D ( 'NONE', #109401, #77073, #94225 ) ;
#56664=CARTESIAN_POINT ( 'NONE',  ( 5.199999999999996625, 0.000000000000000000, -2.700000000000000622 ) ) ;
#57177=EDGE_LOOP ( 'NONE', ( #61642, #180884, #90308, #186342 ) ) ;
#57225=ORIENTED_EDGE ( 'NONE', *, *, #80593, .F. ) ;
#57338=AXIS2_PLACEMENT_3D ( 'NONE', #95220, #153914, #15409 ) ;
#58188=DIRECTION ( 'NONE',  ( -1.000000000000000000, -0.000000000000000000, -0.000000000000000000 ) ) ;
#58624=CARTESIAN_POINT ( 'NONE',  ( 0.2500000000000002220, 0.000000000000000000, 4.250000000000000000 ) ) ;
#58765=DIRECTION ( 'NONE',  ( 1.000000000000000000, 0.000000000000000000, 0.000000000000000000 ) ) ;
#58766=ORIENTED_EDGE ( 'NONE', *, *, #159302, .F. ) ;
#59142=ORIENTED_EDGE ( 'NONE', *, *, #188509, .F. ) ;
#59239=CARTESIAN_POINT ( 'NONE',  ( 2.500000000000000000, -2.357898499370432610, 3.252606517456513302E-15 ) ) ;
#59478=CARTESIAN_POINT ( 'NONE',  ( 2.500000000000000000, -1.178949249685214307, 2.042000000000002036 ) ) ;
#59995=ORIENTED_EDGE ( 'NONE', *, *, #110091, .F. ) ;
#60121=ORIENTED_EDGE ( 'NONE', *, *, #169114, .F. ) ;
#60520=EDGE_LOOP ( 'NONE', ( #147302, #13716, #88566, #193979, #70110 ) ) ;
#60982=EDGE_LOOP ( 'NONE', ( #148956, #82714, #184981 ) ) ;
#61642=ORIENTED_EDGE ( 'NONE', *, *, #170744, .F. ) ;
#62443=ORIENTED_EDGE ( 'NONE', *, *, #75323, .T. ) ;
#62622=DIRECTION ( 'NONE',  ( 0.000000000000000000, 0.000000000000000000, 1.000000000000000000 ) ) ;
#62856=ORIENTED_EDGE ( 'NONE', *, *, #119131, .T. ) ;
#62878=TOROIDAL_SURFACE ( 'NONE', #88590, 2.700000000000000622, 0.2000000000000000111 ) ;
#63370=CARTESIAN_POINT ( 'NONE',  ( 0.000000000000000000, 0.000000000000000000, 0.000000000000000000 ) ) ;
#63401=ORIENTED_EDGE ( 'NONE', *, *, #170744, .T. ) ;
#63407=DIRECTION ( 'NONE',  ( -1.000000000000000000, -0.000000000000000000, -0.000000000000000000 ) ) ;
#63424=DIRECTION ( 'NONE',  ( 0.000000000000000000, 0.8660254037844380415, -0.5000000000000012212 ) ) ;
#63687=ORIENTED_EDGE ( 'NONE', *, *, #197919, .F. ) ;
#63772=VECTOR ( 'NONE', #8778, 1000.000000000000000 ) ;
#64474=EDGE_LOOP ( 'NONE', ( #24675, #87005, #31166, #72917 ) ) ;
#64612=DIRECTION ( 'NONE',  ( -1.000000000000000000, -0.000000000000000000, -0.000000000000000000 ) ) ;
#64714=ORIENTED_EDGE ( 'NONE', *, *, #482, .T. ) ;
#64884=DIRECTION ( 'NONE',  ( -1.000000000000000000, -0.000000000000000000, -0.000000000000000000 ) ) ;
#65086=ORIENTED_EDGE ( 'NONE', *, *, #67045, .T. ) ;
#66031=FACE_OUTER_BOUND ( 'NONE', #146743, .T. ) ;
#66486=PLANE ( 'NONE',  #39751 ) ;
#66587=DIRECTION ( 'NONE',  ( 0.000000000000000000, 0.000000000000000000, 1.000000000000000000 ) ) ;
#66922=VERTEX_POINT ( 'NONE', #149544 ) ;
#67045=EDGE_CURVE ( 'NONE', #92733, #139805, #947, .T. ) ;
#67273=FACE_OUTER_BOUND ( 'NONE', #28412, .T. ) ;
#67283=ADVANCED_FACE ( 'NONE', ( #184990 ), #150886, .T. ) ;
#67444=VERTEX_POINT ( 'NONE', #158613 ) ;
#67595=CARTESIAN_POINT ( 'NONE',  ( 2.500000000000000000, 2.357898499370431722, -2.818925648462311528E-15 ) ) ;
#67790=EDGE_LOOP ( 'NONE', ( #190263, #173129, #62856, #73565, #21569 ) ) ;
#67934=AXIS2_PLACEMENT_3D ( 'NONE', #360, #91364, #152079 ) ;
#68135=LINE ( 'NONE', #19652, #37547 ) ;
#68441=ORIENTED_EDGE ( 'NONE', *, *, #117511, .F. ) ;
#69585=CARTESIAN_POINT ( 'NONE',  ( 5.199999999999996625, 3.306546357697854226E-16, 2.700000000000000622 ) ) ;
#70110=ORIENTED_EDGE ( 'NONE', *, *, #162970, .T. ) ;
#71180=DIRECTION ( 'NONE',  ( -0.5000000000000051070, 0.000000000000000000, 0.8660254037844355990 ) ) ;
#71233=DIRECTION ( 'NONE',  ( 0.000000000000000000, 0.000000000000000000, 1.000000000000000000 ) ) ;
#71290=VECTOR ( 'NONE', #104096, 1000.000000000000000 ) ;
#71388=DIRECTION ( 'NONE',  ( 0.000000000000000000, 0.000000000000000000, 1.000000000000000000 ) ) ;
#71988=ADVANCED_FACE ( 'NONE', ( #157633 ), #95947, .T. ) ;
#72177=CARTESIAN_POINT ( 'NONE',  ( 2.500000000000000000, 0.000000000000000000, 2.041999999999999815 ) ) ;
#72386=CIRCLE ( 'NONE', #185376, 4.250000000000000000 ) ;
#72695=SURFACE_STYLE_USAGE ( .BOTH. , #165699 ) ;
#72917=ORIENTED_EDGE ( 'NONE', *, *, #74806, .F. ) ;
#73142=CARTESIAN_POINT ( 'NONE',  ( 2.500000000000000000, 0.000000000000000000, 0.000000000000000000 ) ) ;
#73565=ORIENTED_EDGE ( 'NONE', *, *, #153660, .T. ) ;
#73686=DIRECTION ( 'NONE',  ( 0.000000000000000000, 0.5000000000000011102, 0.8660254037844380415 ) ) ;
#74082=ADVANCED_FACE ( 'NONE', ( #187266 ), #183319, .T. ) ;
#74575=LINE ( 'NONE', #90716, #44323 ) ;
#74631=FACE_OUTER_BOUND ( 'NONE', #12884, .T. ) ;
#74806=EDGE_CURVE ( 'NONE', #138761, #8238, #54143, .T. ) ;
#75190=EDGE_CURVE ( 'NONE', #139805, #184086, #2452, .T. ) ;
#75323=EDGE_CURVE ( 'NONE', #193525, #120616, #166886, .T. ) ;
#75686=CARTESIAN_POINT ( 'NONE',  ( -31.74999999999995737, 0.000000000000000000, 0.000000000000000000 ) ) ;
#75931=LINE ( 'NONE', #151793, #101664 ) ;
#76325=CARTESIAN_POINT ( 'NONE',  ( 2.500000000000000000, 2.357898499370431722, -2.818925648462311528E-15 ) ) ;
#76779=EDGE_CURVE ( 'NONE', #120616, #88998, #39296, .T. ) ;
#76820=EDGE_LOOP ( 'NONE', ( #26201, #133839 ) ) ;
#76856=VERTEX_POINT ( 'NONE', #51469 ) ;
#76925=VECTOR ( 'NONE', #142283, 1000.000000000000114 ) ;
#76985=DIRECTION ( 'NONE',  ( 0.000000000000000000, 0.000000000000000000, 1.000000000000000000 ) ) ;
#77034=ORIENTED_EDGE ( 'NONE', *, *, #181949, .T. ) ;
#77037=ORIENTED_EDGE ( 'NONE', *, *, #82699, .T. ) ;
#77067=VECTOR ( 'NONE', #94545, 1000.000000000000000 ) ;
#77073=DIRECTION ( 'NONE',  ( 1.000000000000000000, 0.000000000000000000, 0.000000000000000000 ) ) ;
#77595=PLANE ( 'NONE',  #21946 ) ;
#77641=DIRECTION ( 'NONE',  ( -1.000000000000000000, -0.000000000000000000, -0.000000000000000000 ) ) ;
#77656=ORIENTED_EDGE ( 'NONE', *, *, #37032, .T. ) ;
#77798=CARTESIAN_POINT ( 'NONE',  ( 12.99999999999999822, 0.000000000000000000, 0.000000000000000000 ) ) ;
#77849=EDGE_LOOP ( 'NONE', ( #63687, #5649, #158842, #168060 ) ) ;
#77935=LINE ( 'NONE', #186141, #187299 ) ;
#77971=SURFACE_SIDE_STYLE ('',( #16321 ) ) ;
#78051=LINE ( 'NONE', #110387, #135360 ) ;
#78434=ADVANCED_FACE ( 'NONE', ( #15936 ), #77595, .F. ) ;
#78526=PLANE ( 'NONE',  #179871 ) ;
#78540=DIRECTION ( 'NONE',  ( 0.000000000000000000, -0.4999999999999993894, 0.8660254037844389297 ) ) ;
#78961=DIRECTION ( 'NONE',  ( -1.000000000000000000, -0.000000000000000000, -0.000000000000000000 ) ) ;
#78971=DIRECTION ( 'NONE',  ( -1.000000000000000000, -0.000000000000000000, -0.000000000000000000 ) ) ;
#79052=STYLED_ITEM ( 'NONE', ( #117187 ), #22986 ) ;
#79181=COLOUR_RGB ( '', 0.40784314, 0.44705882, 0.49803922) ;
#79657=VECTOR ( 'NONE', #115786, 1000.000000000000000 ) ;
#79954=VECTOR ( 'NONE', #5950, 1000.000000000000114 ) ;
#80129=ORIENTED_EDGE ( 'NONE', *, *, #23510, .F. ) ;
#80371=CARTESIAN_POINT ( 'NONE',  ( 5.199999999999996625, 0.000000000000000000, 2.500000000000000444 ) ) ;
#80593=EDGE_CURVE ( 'NONE', #183244, #88998, #83672, .T. ) ;
#80788=VERTEX_POINT ( 'NONE', #191976 ) ;
#81182=CARTESIAN_POINT ( 'NONE',  ( 2.500000000000000000, -1.178949249685218970, -2.041999999999998039 ) ) ;
#81924=( NAMED_UNIT ( * ) PLANE_ANGLE_UNIT ( ) SI_UNIT ( $, .RADIAN. ) );
#82054=AXIS2_PLACEMENT_3D ( 'NONE', #82060, #99242, #83075 ) ;
#82060=CARTESIAN_POINT ( 'NONE',  ( 0.000000000000000000, 0.000000000000000000, 0.000000000000000000 ) ) ;
#82699=EDGE_CURVE ( 'NONE', #193525, #26587, #96759, .T. ) ;
#82714=ORIENTED_EDGE ( 'NONE', *, *, #30441, .T. ) ;
#82952=VECTOR ( 'NONE', #142044, 1000.000000000000000 ) ;
#83075=DIRECTION ( 'NONE',  ( 1.000000000000000000, 0.000000000000000000, 0.000000000000000000 ) ) ;
#83270=LINE ( 'NONE', #145945, #130864 ) ;
#83507=PLANE ( 'NONE',  #36888 ) ;
#83660=CARTESIAN_POINT ( 'NONE',  ( 0.2500000000000002220, 0.000000000000000000, 4.000000000000000000 ) ) ;
#83672=LINE ( 'NONE', #22020, #99579 ) ;
#84283=UNCERTAINTY_MEASURE_WITH_UNIT (LENGTH_MEASURE( 1.000000000000000082E-05 ), #177880, 'distance_accuracy_value', 'NONE');
#84426=DIRECTION ( 'NONE',  ( 0.000000000000000000, 0.000000000000000000, 1.000000000000000000 ) ) ;
#85392=MECHANICAL_DESIGN_GEOMETRIC_PRESENTATION_REPRESENTATION('',(#101560),#133915);
#85555=( GEOMETRIC_REPRESENTATION_CONTEXT ( 3 ) GLOBAL_UNCERTAINTY_ASSIGNED_CONTEXT ( ( #84283 ) ) GLOBAL_UNIT_ASSIGNED_CONTEXT ( ( #177880, #157716, #118199 ) ) REPRESENTATION_CONTEXT ( 'NONE', 'WORKASPACE' ) );
#85792=FACE_OUTER_BOUND ( 'NONE', #187529, .T. ) ;
#86106=ADVANCED_FACE ( 'NONE', ( #106739 ), #105750, .T. ) ;
#86135=EDGE_CURVE ( 'NONE', #165860, #41053, #186801, .T. ) ;
#86252=CARTESIAN_POINT ( 'NONE',  ( 0.000000000000000000, 5.051668046482832750E-16, -4.000000000000000000 ) ) ;
#86319=VECTOR ( 'NONE', #90025, 1000.000000000000000 ) ;
#86392=CARTESIAN_POINT ( 'NONE',  ( 12.99999999999999822, 0.000000000000000000, 0.000000000000000000 ) ) ;
#87005=ORIENTED_EDGE ( 'NONE', *, *, #190360, .F. ) ;
#87024=EDGE_CURVE ( 'NONE', #45951, #10420, #98511, .T. ) ;
#87516=FACE_OUTER_BOUND ( 'NONE', #193193, .T. ) ;
#87738=CARTESIAN_POINT ( 'NONE',  ( 0.000000000000000000, 2.357898499370431722, -2.818925648462311528E-15 ) ) ;
#88234=ORIENTED_EDGE ( 'NONE', *, *, #10475, .T. ) ;
#88422=ORIENTED_EDGE ( 'NONE', *, *, #7520, .F. ) ;
#88566=ORIENTED_EDGE ( 'NONE', *, *, #11536, .T. ) ;
#88590=AXIS2_PLACEMENT_3D ( 'NONE', #16173, #167867, #92992 ) ;
#88771=ORIENTED_EDGE ( 'NONE', *, *, #162970, .F. ) ;
#88879=DIRECTION ( 'NONE',  ( 0.000000000000000000, 0.000000000000000000, 1.000000000000000000 ) ) ;
#88998=VERTEX_POINT ( 'NONE', #52086 ) ;
#89145=ORIENTED_EDGE ( 'NONE', *, *, #76779, .F. ) ;
#89484=CIRCLE ( 'NONE', #111984, 4.000000000000000000 ) ;
#89587=VERTEX_POINT ( 'NONE', #39916 ) ;
#89832=DIRECTION ( 'NONE',  ( 0.000000000000000000, 0.8660254037844380415, -0.5000000000000011102 ) ) ;
#90025=DIRECTION ( 'NONE',  ( -1.000000000000000000, -0.000000000000000000, -0.000000000000000000 ) ) ;
#90027=CARTESIAN_POINT ( 'NONE',  ( 2.500000000000000000, 1.768423874527822459, -1.021000000000002794 ) ) ;
#90041=DIRECTION ( 'NONE',  ( -1.000000000000000000, -0.000000000000000000, -0.000000000000000000 ) ) ;
#90250=DIRECTION ( 'NONE',  ( -0.5000000000000051070, 1.060575238724903217E-16, -0.8660254037844355990 ) ) ;
#90308=ORIENTED_EDGE ( 'NONE', *, *, #169114, .T. ) ;
#90472=EDGE_CURVE ( 'NONE', #167085, #16610, #180992, .T. ) ;
#90716=CARTESIAN_POINT ( 'NONE',  ( 2.500000000000000000, -1.178949249685214307, 2.042000000000002036 ) ) ;
#90747=ORIENTED_EDGE ( 'NONE', *, *, #198087, .T. ) ;
#90848=DIRECTION ( 'NONE',  ( -1.000000000000000000, -0.000000000000000000, -0.000000000000000000 ) ) ;
#90996=DIRECTION ( 'NONE',  ( 0.000000000000000000, 0.000000000000000000, 1.000000000000000000 ) ) ;
#91364=DIRECTION ( 'NONE',  ( 1.000000000000000000, 0.000000000000000000, 0.000000000000000000 ) ) ;
#92161=EDGE_CURVE ( 'NONE', #171158, #49922, #119273, .T. ) ;
#92400=CARTESIAN_POINT ( 'NONE',  ( 2.500000000000000000, -1.768423874527825124, -1.020999999999998575 ) ) ;
#92733=VERTEX_POINT ( 'NONE', #184907 ) ;
#92992=DIRECTION ( 'NONE',  ( 0.000000000000000000, 0.000000000000000000, -1.000000000000000000 ) ) ;
#93303=ORIENTED_EDGE ( 'NONE', *, *, #190368, .F. ) ;
#93703=FACE_OUTER_BOUND ( 'NONE', #173110, .T. ) ;
#94225=DIRECTION ( 'NONE',  ( 0.000000000000000000, 0.000000000000000000, -1.000000000000000000 ) ) ;
#94545=DIRECTION ( 'NONE',  ( 0.000000000000000000, 0.4999999999999991118, -0.8660254037844391517 ) ) ;
#95220=CARTESIAN_POINT ( 'NONE',  ( 0.2500000000000002220, 0.000000000000000000, 0.000000000000000000 ) ) ;
#95371=DIRECTION ( 'NONE',  ( 0.000000000000000000, -0.5000000000000013323, -0.8660254037844380415 ) ) ;
#95942=EDGE_CURVE ( 'NONE', #41053, #8238, #154836, .T. ) ;
#95947=PLANE ( 'NONE',  #95998 ) ;
#95998=AXIS2_PLACEMENT_3D ( 'NONE', #67595, #144432, #6911 ) ;
#96708=LINE ( 'NONE', #157413, #30149 ) ;
#96759=LINE ( 'NONE', #6747, #76925 ) ;
#97241=ORIENTED_EDGE ( 'NONE', *, *, #169440, .F. ) ;
#97426=DIRECTION ( 'NONE',  ( 0.000000000000000000, -1.000000000000000000, 1.287488025362403787E-15 ) ) ;
#97793=DIRECTION ( 'NONE',  ( 0.000000000000000000, 0.000000000000000000, -1.000000000000000000 ) ) ;
#98071=AXIS2_PLACEMENT_3D ( 'NONE', #28402, #90041, #9231 ) ;
#98173=DIRECTION ( 'NONE',  ( 0.000000000000000000, 0.000000000000000000, 1.000000000000000000 ) ) ;
#98177=FACE_OUTER_BOUND ( 'NONE', #178181, .T. ) ;
#98258=VERTEX_POINT ( 'NONE', #86252 ) ;
#98511=LINE ( 'NONE', #175377, #77067 ) ;
#98595=CIRCLE ( 'NONE', #137297, 2.700000000000000622 ) ;
#98692=PRODUCT ( 'socket head cap screw_iso_ISO 4762 M5 x 8 - 8N', 'socket head cap screw_iso_ISO 4762 M5 x 8 - 8N', '', ( #128110 ) ) ;
#98973=LINE ( 'NONE', #193011, #137578 ) ;
#99139=AXIS2_PLACEMENT_3D ( 'NONE', #69585, #22086, #161593 ) ;
#99242=DIRECTION ( 'NONE',  ( 0.000000000000000000, 0.000000000000000000, 1.000000000000000000 ) ) ;
#99579=VECTOR ( 'NONE', #132190, 1000.000000000000000 ) ;
#100218=DIRECTION ( 'NONE',  ( -0.000000000000000000, 1.000000000000000000, 1.224646799147353207E-16 ) ) ;
#100462=UNCERTAINTY_MEASURE_WITH_UNIT (LENGTH_MEASURE( 1.000000000000000082E-05 ), #126467, 'distance_accuracy_value', 'NONE');
#100590=VERTEX_POINT ( 'NONE', #22504 ) ;
#100601=LINE ( 'NONE', #131952, #79657 ) ;
#100678=DIRECTION ( 'NONE',  ( 0.000000000000000000, 0.000000000000000000, -1.000000000000000000 ) ) ;
#101007=FILL_AREA_STYLE ('',( #56520 ) ) ;
#101560=STYLED_ITEM ( 'NONE', ( #49638 ), #11768 ) ;
#101588=VERTEX_POINT ( 'NONE', #192000 ) ;
#101611=VECTOR ( 'NONE', #77641, 1000.000000000000000 ) ;
#101664=VECTOR ( 'NONE', #107256, 1000.000000000000000 ) ;
#101685=FACE_OUTER_BOUND ( 'NONE', #130495, .T. ) ;
#101715=CIRCLE ( 'NONE', #117898, 0.2500000000000002220 ) ;
#101937=AXIS2_PLACEMENT_3D ( 'NONE', #109314, #78971, #76985 ) ;
#102004=ADVANCED_FACE ( 'NONE', ( #190022, #51496 ), #174846, .T. ) ;
#102032=ORIENTED_EDGE ( 'NONE', *, *, #187359, .F. ) ;
#102325=EDGE_LOOP ( 'NONE', ( #90747, #63401, #153233, #60121 ) ) ;
#102339=AXIS2_PLACEMENT_3D ( 'NONE', #158597, #64612, #66587 ) ;
#102673=EDGE_LOOP ( 'NONE', ( #131560, #50745, #152600, #143286 ) ) ;
#103218=CARTESIAN_POINT ( 'NONE',  ( 2.500000000000000000, 2.357898499370431722, -2.818925648462311528E-15 ) ) ;
#104015=DIRECTION ( 'NONE',  ( 0.000000000000000000, 0.000000000000000000, -1.000000000000000000 ) ) ;
#104020=SURFACE_STYLE_FILL_AREA ( #101007 ) ;
#104096=DIRECTION ( 'NONE',  ( 0.000000000000000000, -1.000000000000000000, 1.287488025362403787E-15 ) ) ;
#104411=ORIENTED_EDGE ( 'NONE', *, *, #176185, .T. ) ;
#104504=ORIENTED_EDGE ( 'NONE', *, *, #76779, .T. ) ;
#104571=CIRCLE ( 'NONE', #107854, 2.055000000000000160 ) ;
#104609=CARTESIAN_POINT ( 'NONE',  ( 5.199999999999996625, 0.000000000000000000, 0.000000000000000000 ) ) ;
#104763=DIRECTION ( 'NONE',  ( 0.000000000000000000, -0.4999999999999991118, 0.8660254037844390407 ) ) ;
#104775=CARTESIAN_POINT ( 'NONE',  ( 0.000000000000000000, -1.178949249685214307, 2.042000000000002036 ) ) ;
#104912=DIRECTION ( 'NONE',  ( 0.000000000000000000, -0.5000000000000011102, -0.8660254037844379305 ) ) ;
#105014=SHAPE_REPRESENTATION_RELATIONSHIP ( 'NONE' , 'NONE' ,  #9542, #22986 ) ;
#105550=DIRECTION ( 'NONE',  ( 0.000000000000000000, 1.000000000000000000, -1.471414886128461669E-15 ) ) ;
#105750=PLANE ( 'NONE',  #160925 ) ;
#106417=PLANE ( 'NONE',  #56564 ) ;
#106535=CARTESIAN_POINT ( 'NONE',  ( 0.000000000000000000, 0.000000000000000000, 4.000000000000000000 ) ) ;
#106739=FACE_OUTER_BOUND ( 'NONE', #139317, .T. ) ;
#107153=EDGE_LOOP ( 'NONE', ( #77034, #31839, #132041 ) ) ;
#107246=ORIENTED_EDGE ( 'NONE', *, *, #197919, .T. ) ;
#107256=DIRECTION ( 'NONE',  ( 0.000000000000000000, 1.000000000000000000, -1.471414886128461669E-15 ) ) ;
#107734=ADVANCED_FACE ( 'NONE', ( #122189 ), #27230, .T. ) ;
#107774=CIRCLE ( 'NONE', #110953, 0.2500000000000002220 ) ;
#107854=AXIS2_PLACEMENT_3D ( 'NONE', #29215, #90848, #88879 ) ;
#107988=EDGE_CURVE ( 'NONE', #92733, #168893, #104571, .T. ) ;
#108101=EDGE_CURVE ( 'NONE', #67444, #38560, #72386, .T. ) ;
#108242=ADVANCED_FACE ( 'NONE', ( #131903 ), #124015, .T. ) ;
#109048=ADVANCED_FACE ( 'NONE', ( #4797 ), #66486, .F. ) ;
#109314=CARTESIAN_POINT ( 'NONE',  ( 2.500000000000000000, 0.000000000000000000, 0.000000000000000000 ) ) ;
#109366=DIRECTION ( 'NONE',  ( -1.000000000000000000, -0.000000000000000000, -0.000000000000000000 ) ) ;
#109401=CARTESIAN_POINT ( 'NONE',  ( 2.500000000000000000, 2.357898499370431722, -2.818925648462311528E-15 ) ) ;
#109675=CARTESIAN_POINT ( 'NONE',  ( -31.74999999999995737, 0.000000000000000000, 0.000000000000000000 ) ) ;
#110091=EDGE_CURVE ( 'NONE', #16610, #167085, #142927, .T. ) ;
#110387=CARTESIAN_POINT ( 'NONE',  ( 0.000000000000000000, -2.357898499370432610, 3.252606517456513302E-15 ) ) ;
#110953=AXIS2_PLACEMENT_3D ( 'NONE', #192245, #100218, #8218 ) ;
#111386=( GEOMETRIC_REPRESENTATION_CONTEXT ( 3 ) GLOBAL_UNCERTAINTY_ASSIGNED_CONTEXT ( ( #5450 ) ) GLOBAL_UNIT_ASSIGNED_CONTEXT ( ( #162691, #120174, #196055 ) ) REPRESENTATION_CONTEXT ( 'NONE', 'WORKASPACE' ) );
#111522=CLOSED_SHELL ( 'NONE', ( #2768, #124493, #4122, #67283, #190608, #41538, #183853, #20622, #102004, #107734, #108242, #14106, #168748, #74082, #71988, #56314, #22134, #86106, #147858, #78434, #49489, #167639, #17771, #25683, #18733, #109048, #150283 ) ) ;
#111860=DIRECTION ( 'NONE',  ( -1.000000000000000000, 0.000000000000000000, -0.000000000000000000 ) ) ;
#111984=AXIS2_PLACEMENT_3D ( 'NONE', #55108, #179482, #84426 ) ;
#112379=DIRECTION ( 'NONE',  ( 0.000000000000000000, 0.000000000000000000, 1.000000000000000000 ) ) ;
#112435=EDGE_LOOP ( 'NONE', ( #77656, #20439, #104504, #117892, #9419, #151815 ) ) ;
#112871=DIRECTION ( 'NONE',  ( 0.000000000000000000, 0.000000000000000000, 1.000000000000000000 ) ) ;
#113885=EDGE_CURVE ( 'NONE', #80788, #167413, #182406, .T. ) ;
#114470=CARTESIAN_POINT ( 'NONE',  ( 0.2500000000000002220, 0.000000000000000000, 0.000000000000000000 ) ) ;
#114545=VECTOR ( 'NONE', #28735, 1000.000000000000000 ) ;
#114695=CIRCLE ( 'NONE', #27569, 2.041999999999999815 ) ;
#114885=DIRECTION ( 'NONE',  ( -1.000000000000000000, -0.000000000000000000, -0.000000000000000000 ) ) ;
#114960=ORIENTED_EDGE ( 'NONE', *, *, #123771, .F. ) ;
#115067=CARTESIAN_POINT ( 'NONE',  ( 0.000000000000000000, 2.357898499370431722, -2.818925648462311528E-15 ) ) ;
#115597=VECTOR ( 'NONE', #71180, 1000.000000000000114 ) ;
#115786=DIRECTION ( 'NONE',  ( -1.000000000000000000, -0.000000000000000000, -0.000000000000000000 ) ) ;
#117115=LINE ( 'NONE', #53446, #156885 ) ;
#117187=PRESENTATION_STYLE_ASSIGNMENT (( #72695 ) ) ;
#117386=CARTESIAN_POINT ( 'NONE',  ( 2.500000000000000000, 0.000000000000000000, 0.000000000000000000 ) ) ;
#117511=EDGE_CURVE ( 'NONE', #183244, #45951, #77935, .T. ) ;
#117788=DIRECTION ( 'NONE',  ( 0.000000000000000000, 0.000000000000000000, -1.000000000000000000 ) ) ;
#117865=VECTOR ( 'NONE', #22062, 1000.000000000000114 ) ;
#117892=ORIENTED_EDGE ( 'NONE', *, *, #123771, .T. ) ;
#117898=AXIS2_PLACEMENT_3D ( 'NONE', #83660, #173712, #36163 ) ;
#118199=( NAMED_UNIT ( * ) SI_UNIT ( $, .STERADIAN. ) SOLID_ANGLE_UNIT ( ) );
#118337=DIRECTION ( 'NONE',  ( 0.000000000000000000, -1.000000000000000000, 0.000000000000000000 ) ) ;
#118468=PLANE ( 'NONE',  #16770 ) ;
#118518=CIRCLE ( 'NONE', #99139, 0.2000000000000000944 ) ;
#118854=ORIENTED_EDGE ( 'NONE', *, *, #113885, .F. ) ;
#119131=EDGE_CURVE ( 'NONE', #100590, #101588, #170570, .T. ) ;
#119173=DIRECTION ( 'NONE',  ( 1.000000000000000000, 0.000000000000000000, 0.000000000000000000 ) ) ;
#119206=ORIENTED_EDGE ( 'NONE', *, *, #86135, .F. ) ;
#119273=LINE ( 'NONE', #42433, #71290 ) ;
#120174=( NAMED_UNIT ( * ) PLANE_ANGLE_UNIT ( ) SI_UNIT ( $, .RADIAN. ) );
#120357=DIRECTION ( 'NONE',  ( -1.000000000000000000, -0.000000000000000000, -0.000000000000000000 ) ) ;
#120476=EDGE_CURVE ( 'NONE', #4163, #76856, #28864, .T. ) ;
#120616=VERTEX_POINT ( 'NONE', #27878 ) ;
#120908=DIRECTION ( 'NONE',  ( -0.000000000000000000, 0.8660254037844391517, 0.4999999999999991673 ) ) ;
#121037=CIRCLE ( 'NONE', #30692, 2.041999999999999815 ) ;
#121374=ORIENTED_EDGE ( 'NONE', *, *, #159302, .T. ) ;
#122189=FACE_OUTER_BOUND ( 'NONE', #57177, .T. ) ;
#122312=CARTESIAN_POINT ( 'NONE',  ( 12.99999999999999822, 2.516649172247811061E-16, -2.055000000000000160 ) ) ;
#122482=CARTESIAN_POINT ( 'NONE',  ( 2.500000000000000000, 0.000000000000000000, 0.000000000000000000 ) ) ;
#123771=EDGE_CURVE ( 'NONE', #88998, #49922, #78051, .T. ) ;
#124015=CONICAL_SURFACE ( 'NONE', #11050, 2.055000000000000160, 0.7853981633974712606 ) ;
#124493=ADVANCED_FACE ( 'NONE', ( #98177 ), #161154, .T. ) ;
#124679=VECTOR ( 'NONE', #90250, 1000.000000000000114 ) ;
#124731=DIRECTION ( 'NONE',  ( -1.000000000000000000, -0.000000000000000000, -0.000000000000000000 ) ) ;
#124829=AXIS2_PLACEMENT_3D ( 'NONE', #122482, #78961, #43675 ) ;
#124846=DIRECTION ( 'NONE',  ( -1.000000000000000000, -0.000000000000000000, -0.000000000000000000 ) ) ;
#125154=ORIENTED_EDGE ( 'NONE', *, *, #30441, .F. ) ;
#125535=EDGE_LOOP ( 'NONE', ( #125590, #152253, #64714, #198841, #6505 ) ) ;
#125590=ORIENTED_EDGE ( 'NONE', *, *, #175617, .F. ) ;
#125969=CARTESIAN_POINT ( 'NONE',  ( 2.500000000000000000, 2.357898499370431722, -2.818925648462311528E-15 ) ) ;
#126038=FACE_BOUND ( 'NONE', #112435, .T. ) ;
#126134=CARTESIAN_POINT ( 'NONE',  ( 0.000000000000000000, -1.178949249685218970, -2.041999999999998039 ) ) ;
#126467=( LENGTH_UNIT ( ) NAMED_UNIT ( * ) SI_UNIT ( .MILLI., .METRE. ) );
#127014=CARTESIAN_POINT ( 'NONE',  ( 12.55500000000001748, 0.000000000000000000, 2.500000000000000444 ) ) ;
#127049=DIRECTION ( 'NONE',  ( 1.000000000000000000, 0.000000000000000000, 0.000000000000000000 ) ) ;
#127361=CIRCLE ( 'NONE', #40205, 2.041999999999999815 ) ;
#127514=DIRECTION ( 'NONE',  ( 0.000000000000000000, 0.000000000000000000, -1.000000000000000000 ) ) ;
#127621=FACE_OUTER_BOUND ( 'NONE', #52984, .T. ) ;
#128110=PRODUCT_CONTEXT ( 'NONE', #175865, 'mechanical' ) ;
#128149=DIRECTION ( 'NONE',  ( 1.000000000000000000, 0.000000000000000000, 0.000000000000000000 ) ) ;
#128532=CARTESIAN_POINT ( 'NONE',  ( 4.999999999999999112, 0.000000000000000000, 0.000000000000000000 ) ) ;
#130153=CARTESIAN_POINT ( 'NONE',  ( 4.999999999999997335, 0.000000000000000000, -2.700000000000000622 ) ) ;
#130495=EDGE_LOOP ( 'NONE', ( #102032, #174043 ) ) ;
#130540=DIRECTION ( 'NONE',  ( 0.000000000000000000, 0.000000000000000000, 1.000000000000000000 ) ) ;
#130864=VECTOR ( 'NONE', #97426, 1000.000000000000000 ) ;
#130994=ORIENTED_EDGE ( 'NONE', *, *, #110091, .T. ) ;
#131560=ORIENTED_EDGE ( 'NONE', *, *, #67045, .F. ) ;
#131903=FACE_OUTER_BOUND ( 'NONE', #102673, .T. ) ;
#131952=CARTESIAN_POINT ( 'NONE',  ( -31.74999999999995737, 0.000000000000000000, 2.500000000000000444 ) ) ;
#132041=ORIENTED_EDGE ( 'NONE', *, *, #482, .F. ) ;
#132190=DIRECTION ( 'NONE',  ( -1.000000000000000000, -0.000000000000000000, -0.000000000000000000 ) ) ;
#133535=CARTESIAN_POINT ( 'NONE',  ( 4.999999999999997335, 0.000000000000000000, 0.000000000000000000 ) ) ;
#133659=ORIENTED_EDGE ( 'NONE', *, *, #182855, .T. ) ;
#133839=ORIENTED_EDGE ( 'NONE', *, *, #172288, .F. ) ;
#133915=( GEOMETRIC_REPRESENTATION_CONTEXT ( 3 ) GLOBAL_UNCERTAINTY_ASSIGNED_CONTEXT ( ( #100462 ) ) GLOBAL_UNIT_ASSIGNED_CONTEXT ( ( #126467, #81924, #157816 ) ) REPRESENTATION_CONTEXT ( 'NONE', 'WORKASPACE' ) );
#134223=CONICAL_SURFACE ( 'NONE', #49752, 2.041999999999999815, 1.047197551196591858 ) ;
#134406=DIRECTION ( 'NONE',  ( -1.000000000000000000, -0.000000000000000000, -0.000000000000000000 ) ) ;
#134669=AXIS2_PLACEMENT_3D ( 'NONE', #104609, #10620, #117788 ) ;
#135007=ORIENTED_EDGE ( 'NONE', *, *, #187359, .T. ) ;
#135360=VECTOR ( 'NONE', #33556, 1000.000000000000000 ) ;
#135557=FACE_OUTER_BOUND ( 'NONE', #181040, .T. ) ;
#136274=ORIENTED_EDGE ( 'NONE', *, *, #108101, .T. ) ;
#136550=EDGE_CURVE ( 'NONE', #26587, #80788, #127361, .T. ) ;
#136651=AXIS2_PLACEMENT_3D ( 'NONE', #1729, #63407, #186780 ) ;
#137256=PRODUCT_DEFINITION_SHAPE ( 'NONE', 'NONE',  #189524 ) ;
#137297=AXIS2_PLACEMENT_3D ( 'NONE', #143678, #109366, #127514 ) ;
#137578=VECTOR ( 'NONE', #194022, 1000.000000000000114 ) ;
#137629=DIRECTION ( 'NONE',  ( 0.000000000000000000, 0.4999999999999991118, -0.8660254037844391517 ) ) ;
#137833=VERTEX_POINT ( 'NONE', #87738 ) ;
#137966=AXIS2_PLACEMENT_3D ( 'NONE', #133535, #193223, #98173 ) ;
#137990=AXIS2_PLACEMENT_3D ( 'NONE', #181070, #120357, #90996 ) ;
#138761=VERTEX_POINT ( 'NONE', #45230 ) ;
#139102=CARTESIAN_POINT ( 'NONE',  ( 4.999999999999997335, 5.204748896376250699E-16, -4.250000000000000000 ) ) ;
#139266=CARTESIAN_POINT ( 'NONE',  ( 2.500000000000000000, 2.357898499370431722, -2.818925648462311528E-15 ) ) ;
#139317=EDGE_LOOP ( 'NONE', ( #114960, #57225, #159935, #157687, #5156 ) ) ;
#139638=SURFACE_STYLE_USAGE ( .BOTH. , #77971 ) ;
#139778=VERTEX_POINT ( 'NONE', #164780 ) ;
#139805=VERTEX_POINT ( 'NONE', #198096 ) ;
#139960=CIRCLE ( 'NONE', #13980, 2.500000000000000444 ) ;
#140236=FACE_OUTER_BOUND ( 'NONE', #102325, .T. ) ;
#140643=DIRECTION ( 'NONE',  ( -1.000000000000000000, -0.000000000000000000, -0.000000000000000000 ) ) ;
#141135=DIRECTION ( 'NONE',  ( 0.000000000000000000, 0.000000000000000000, -1.000000000000000000 ) ) ;
#141273=CIRCLE ( 'NONE', #137966, 4.250000000000000000 ) ;
#141729=DIRECTION ( 'NONE',  ( 0.000000000000000000, -1.000000000000000000, 1.471414886128461471E-15 ) ) ;
#142044=DIRECTION ( 'NONE',  ( -1.000000000000000000, -0.000000000000000000, -0.000000000000000000 ) ) ;
#142226=DIRECTION ( 'NONE',  ( 0.000000000000000000, 0.000000000000000000, -1.000000000000000000 ) ) ;
#142283=DIRECTION ( 'NONE',  ( 0.000000000000000000, -0.5000000000000011102, -0.8660254037844379305 ) ) ;
#142538=DIRECTION ( 'NONE',  ( -1.000000000000000000, -0.000000000000000000, -0.000000000000000000 ) ) ;
#142927=CIRCLE ( 'NONE', #197951, 4.250000000000000000 ) ;
#143286=ORIENTED_EDGE ( 'NONE', *, *, #75190, .F. ) ;
#143405=AXIS2_PLACEMENT_3D ( 'NONE', #73142, #152923, #11471 ) ;
#143579=AXIS2_PLACEMENT_3D ( 'NONE', #144512, #168652, #104015 ) ;
#143659=APPLICATION_CONTEXT ( 'automotive_design' ) ;
#143678=CARTESIAN_POINT ( 'NONE',  ( 4.999999999999999112, 0.000000000000000000, 0.000000000000000000 ) ) ;
#143706=PRODUCT_DEFINITION_FORMATION_WITH_SPECIFIED_SOURCE ( 'ANY', '', #98692, .NOT_KNOWN. ) ;
#144432=DIRECTION ( 'NONE',  ( 0.000000000000000000, -0.8660254037844390407, -0.4999999999999994449 ) ) ;
#144465=CARTESIAN_POINT ( 'NONE',  ( 0.000000000000000000, -1.178949249685214307, 2.042000000000002036 ) ) ;
#144512=CARTESIAN_POINT ( 'NONE',  ( 2.500000000000000000, 2.357898499370431722, -2.818925648462311528E-15 ) ) ;
#144944=CARTESIAN_POINT ( 'NONE',  ( 0.2500000000000002220, 5.204748896376250699E-16, -4.250000000000000000 ) ) ;
#145481=EDGE_CURVE ( 'NONE', #45951, #26587, #121037, .T. ) ;
#145945=CARTESIAN_POINT ( 'NONE',  ( 2.500000000000000000, 1.178949249685212974, -2.042000000000001148 ) ) ;
#146182=DIRECTION ( 'NONE',  ( 1.000000000000000000, 0.000000000000000000, 0.000000000000000000 ) ) ;
#146519=CARTESIAN_POINT ( 'NONE',  ( -31.74999999999995737, 3.061616997868383634E-16, -2.500000000000000444 ) ) ;
#146743=EDGE_LOOP ( 'NONE', ( #159378, #194055, #28376, #164216, #196074 ) ) ;
#147302=ORIENTED_EDGE ( 'NONE', *, *, #186961, .F. ) ;
#147478=PLANE ( 'NONE',  #163096 ) ;
#147858=ADVANCED_FACE ( 'NONE', ( #66031 ), #1370, .F. ) ;
#148227=ORIENTED_EDGE ( 'NONE', *, *, #120476, .F. ) ;
#148956=ORIENTED_EDGE ( 'NONE', *, *, #82699, .F. ) ;
#149204=DIRECTION ( 'NONE',  ( 0.000000000000000000, 0.000000000000000000, 1.000000000000000000 ) ) ;
#149544=CARTESIAN_POINT ( 'NONE',  ( 0.000000000000000000, 1.178949249685217193, 2.041999999999998483 ) ) ;
#149771=ORIENTED_EDGE ( 'NONE', *, *, #11536, .F. ) ;
#150283=ADVANCED_FACE ( 'NONE', ( #186181 ), #189119, .F. ) ;
#150298=LINE ( 'NONE', #104775, #63772 ) ;
#150416=VECTOR ( 'NONE', #4904, 1000.000000000000000 ) ;
#150571=CARTESIAN_POINT ( 'NONE',  ( 4.999999999999997335, 0.000000000000000000, 0.000000000000000000 ) ) ;
#150886=CONICAL_SURFACE ( 'NONE', #176712, 2.055000000000000160, 0.7853981633974712606 ) ;
#151512=FACE_OUTER_BOUND ( 'NONE', #168359, .T. ) ;
#151672=EDGE_CURVE ( 'NONE', #76856, #171158, #68135, .T. ) ;
#151793=CARTESIAN_POINT ( 'NONE',  ( 2.500000000000000000, -1.178949249685214307, 2.042000000000002036 ) ) ;
#151815=ORIENTED_EDGE ( 'NONE', *, *, #10475, .F. ) ;
#152079=DIRECTION ( 'NONE',  ( 0.000000000000000000, 0.000000000000000000, 1.000000000000000000 ) ) ;
#152253=ORIENTED_EDGE ( 'NONE', *, *, #186961, .T. ) ;
#152533=DIRECTION ( 'NONE',  ( 0.000000000000000000, 0.000000000000000000, 1.000000000000000000 ) ) ;
#152600=ORIENTED_EDGE ( 'NONE', *, *, #188509, .T. ) ;
#152923=DIRECTION ( 'NONE',  ( -1.000000000000000000, -0.000000000000000000, -0.000000000000000000 ) ) ;
#153233=ORIENTED_EDGE ( 'NONE', *, *, #190360, .T. ) ;
#153660=EDGE_CURVE ( 'NONE', #101588, #167413, #98973, .T. ) ;
#153758=CARTESIAN_POINT ( 'NONE',  ( 2.500000000000000000, -1.768423874527823569, 1.021000000000002794 ) ) ;
#153914=DIRECTION ( 'NONE',  ( -1.000000000000000000, -0.000000000000000000, -0.000000000000000000 ) ) ;
#154726=LINE ( 'NONE', #72177, #115597 ) ;
#154836=CIRCLE ( 'NONE', #187194, 0.2000000000000000944 ) ;
#155072=LINE ( 'NONE', #47905, #18326 ) ;
#155906=FACE_OUTER_BOUND ( 'NONE', #60982, .T. ) ;
#156411=CYLINDRICAL_SURFACE ( 'NONE', #136651, 2.500000000000000444 ) ;
#156656=ORIENTED_EDGE ( 'NONE', *, *, #176185, .F. ) ;
#156885=VECTOR ( 'NONE', #41289, 1000.000000000000114 ) ;
#157413=CARTESIAN_POINT ( 'NONE',  ( -31.74999999999995737, 0.000000000000000000, 4.250000000000000000 ) ) ;
#157633=FACE_OUTER_BOUND ( 'NONE', #67790, .T. ) ;
#157687=ORIENTED_EDGE ( 'NONE', *, *, #87024, .T. ) ;
#157716=( NAMED_UNIT ( * ) PLANE_ANGLE_UNIT ( ) SI_UNIT ( $, .RADIAN. ) );
#157759=AXIS2_PLACEMENT_3D ( 'NONE', #31897, #182607, #28933 ) ;
#157816=( NAMED_UNIT ( * ) SI_UNIT ( $, .STERADIAN. ) SOLID_ANGLE_UNIT ( ) );
#158162=CYLINDRICAL_SURFACE ( 'NONE', #185879, 4.250000000000000000 ) ;
#158386=DIRECTION ( 'NONE',  ( -1.000000000000000000, -0.000000000000000000, -0.000000000000000000 ) ) ;
#158597=CARTESIAN_POINT ( 'NONE',  ( 0.000000000000000000, 0.000000000000000000, 0.000000000000000000 ) ) ;
#158613=CARTESIAN_POINT ( 'NONE',  ( 4.999999999999997335, 0.000000000000000000, 4.250000000000000000 ) ) ;
#158842=ORIENTED_EDGE ( 'NONE', *, *, #8681, .T. ) ;
#159302=EDGE_CURVE ( 'NONE', #8238, #138761, #98595, .T. ) ;
#159378=ORIENTED_EDGE ( 'NONE', *, *, #92161, .T. ) ;
#159935=ORIENTED_EDGE ( 'NONE', *, *, #117511, .T. ) ;
#160382=CARTESIAN_POINT ( 'NONE',  ( 2.500000000000000000, 0.000000000000000000, 0.000000000000000000 ) ) ;
#160925=AXIS2_PLACEMENT_3D ( 'NONE', #59239, #120908, #104763 ) ;
#161154=TOROIDAL_SURFACE ( 'NONE', #177347, 4.000000000000000000, 0.2500000000000000000 ) ;
#161593=DIRECTION ( 'NONE',  ( 0.000000000000000000, 1.224646799147353207E-16, 1.000000000000000000 ) ) ;
#161700=LINE ( 'NONE', #146519, #192822 ) ;
#162691=( LENGTH_UNIT ( ) NAMED_UNIT ( * ) SI_UNIT ( .MILLI., .METRE. ) );
#162970=EDGE_CURVE ( 'NONE', #4163, #89587, #11869, .T. ) ;
#163096=AXIS2_PLACEMENT_3D ( 'NONE', #8968, #18410, #141729 ) ;
#164216=ORIENTED_EDGE ( 'NONE', *, *, #16052, .F. ) ;
#164780=CARTESIAN_POINT ( 'NONE',  ( 3.678949249685231848, 1.601138781673192758E-19, 0.000000000000000000 ) ) ;
#165004=DIRECTION ( 'NONE',  ( 1.000000000000000000, 0.000000000000000000, 0.000000000000000000 ) ) ;
#165699=SURFACE_SIDE_STYLE ('',( #104020 ) ) ;
#165742=AXIS2_PLACEMENT_3D ( 'NONE', #22885, #114885, #71388 ) ;
#165860=VERTEX_POINT ( 'NONE', #80371 ) ;
#165915=EDGE_CURVE ( 'NONE', #10420, #49922, #52028, .T. ) ;
#166413=AXIS2_PLACEMENT_3D ( 'NONE', #103218, #193234, #27390 ) ;
#166886=LINE ( 'NONE', #28387, #86319 ) ;
#167085=VERTEX_POINT ( 'NONE', #58624 ) ;
#167413=VERTEX_POINT ( 'NONE', #197208 ) ;
#167582=CARTESIAN_POINT ( 'NONE',  ( 2.500000000000000000, -2.357898499370432610, 3.252606517456513302E-15 ) ) ;
#167611=ORIENTED_EDGE ( 'NONE', *, *, #169440, .T. ) ;
#167639=ADVANCED_FACE ( 'NONE', ( #67273 ), #191619, .F. ) ;
#167818=DIRECTION ( 'NONE',  ( -1.000000000000000000, -0.000000000000000000, -0.000000000000000000 ) ) ;
#167867=DIRECTION ( 'NONE',  ( 1.000000000000000000, 0.000000000000000000, 0.000000000000000000 ) ) ;
#168060=ORIENTED_EDGE ( 'NONE', *, *, #168230, .F. ) ;
#168230=EDGE_CURVE ( 'NONE', #98258, #7157, #89484, .T. ) ;
#168359=EDGE_LOOP ( 'NONE', ( #89145, #17985, #77037, #133659, #178125 ) ) ;
#168652=DIRECTION ( 'NONE',  ( 1.000000000000000000, 0.000000000000000000, 0.000000000000000000 ) ) ;
#168748=ADVANCED_FACE ( 'NONE', ( #177475 ), #170150, .F. ) ;
#168790=DIRECTION ( 'NONE',  ( 0.000000000000000000, 0.000000000000000000, 1.000000000000000000 ) ) ;
#168893=VERTEX_POINT ( 'NONE', #22778 ) ;
#169114=EDGE_CURVE ( 'NONE', #184086, #165860, #100601, .T. ) ;
#169200=AXIS2_PLACEMENT_3D ( 'NONE', #75686, #134406, #196093 ) ;
#169409=COLOUR_RGB ( '', 0.40784314, 0.44705882, 0.49803922) ;
#169440=EDGE_CURVE ( 'NONE', #38560, #16610, #155072, .T. ) ;
#169670=EDGE_LOOP ( 'NONE', ( #88234, #190620, #148227, #156656, #195290 ) ) ;
#170150=TOROIDAL_SURFACE ( 'NONE', #134669, 2.700000000000000622, 0.2000000000000000111 ) ;
#170272=ORIENTED_EDGE ( 'NONE', *, *, #145481, .F. ) ;
#170570=LINE ( 'NONE', #187749, #22603 ) ;
#170744=EDGE_CURVE ( 'NONE', #139805, #41053, #161700, .T. ) ;
#171158=VERTEX_POINT ( 'NONE', #192455 ) ;
#172288=EDGE_CURVE ( 'NONE', #38560, #67444, #141273, .T. ) ;
#173055=CIRCLE ( 'NONE', #53532, 2.055000000000000160 ) ;
#173110=EDGE_LOOP ( 'NONE', ( #23413, #23489 ) ) ;
#173129=ORIENTED_EDGE ( 'NONE', *, *, #50044, .F. ) ;
#173336=EDGE_CURVE ( 'NONE', #120616, #66922, #150298, .T. ) ;
#173712=DIRECTION ( 'NONE',  ( 0.000000000000000000, -1.000000000000000000, 0.000000000000000000 ) ) ;
#174043=ORIENTED_EDGE ( 'NONE', *, *, #107988, .F. ) ;
#174224=LINE ( 'NONE', #51857, #182418 ) ;
#174296=VECTOR ( 'NONE', #180566, 999.9999999999997726 ) ;
#174337=DIRECTION ( 'NONE',  ( -1.000000000000000000, -0.000000000000000000, -0.000000000000000000 ) ) ;
#174676=CARTESIAN_POINT ( 'NONE',  ( 2.500000000000000000, 2.357898499370431722, -2.818925648462311528E-15 ) ) ;
#174696=ORIENTED_EDGE ( 'NONE', *, *, #120476, .T. ) ;
#174846=PLANE ( 'NONE',  #3142 ) ;
#175377=CARTESIAN_POINT ( 'NONE',  ( 2.500000000000000000, -2.357898499370432610, 3.252606517456513302E-15 ) ) ;
#175460=DIRECTION ( 'NONE',  ( 1.000000000000000000, 0.000000000000000000, 0.000000000000000000 ) ) ;
#175617=EDGE_CURVE ( 'NONE', #139778, #80788, #154726, .T. ) ;
#175865=APPLICATION_CONTEXT ( 'automotive_design' ) ;
#176185=EDGE_CURVE ( 'NONE', #100590, #4163, #5002, .T. ) ;
#176680=CIRCLE ( 'NONE', #102339, 4.000000000000000000 ) ;
#176712=AXIS2_PLACEMENT_3D ( 'NONE', #77798, #46474, #62622 ) ;
#177347=AXIS2_PLACEMENT_3D ( 'NONE', #18400, #64884, #112379 ) ;
#177475=FACE_OUTER_BOUND ( 'NONE', #64474, .T. ) ;
#177880=( LENGTH_UNIT ( ) NAMED_UNIT ( * ) SI_UNIT ( .MILLI., .METRE. ) );
#178125=ORIENTED_EDGE ( 'NONE', *, *, #80593, .T. ) ;
#178181=EDGE_LOOP ( 'NONE', ( #59995, #107246, #9951, #5268 ) ) ;
#179429=DIRECTION ( 'NONE',  ( -1.000000000000000000, -0.000000000000000000, -0.000000000000000000 ) ) ;
#179482=DIRECTION ( 'NONE',  ( -1.000000000000000000, -0.000000000000000000, -0.000000000000000000 ) ) ;
#179871=AXIS2_PLACEMENT_3D ( 'NONE', #63370, #111860, #15884 ) ;
#180136=ORIENTED_EDGE ( 'NONE', *, *, #119131, .F. ) ;
#180566=DIRECTION ( 'NONE',  ( 0.000000000000000000, -0.5000000000000013323, -0.8660254037844380415 ) ) ;
#180583=ORIENTED_EDGE ( 'NONE', *, *, #172288, .T. ) ;
#180884=ORIENTED_EDGE ( 'NONE', *, *, #75190, .T. ) ;
#180992=CIRCLE ( 'NONE', #67934, 4.250000000000000000 ) ;
#181040=EDGE_LOOP ( 'NONE', ( #180136, #104411, #80129 ) ) ;
#181070=CARTESIAN_POINT ( 'NONE',  ( 12.55500000000001748, 0.000000000000000000, 0.000000000000000000 ) ) ;
#181147=DIRECTION ( 'NONE',  ( 0.000000000000000000, 0.000000000000000000, -1.000000000000000000 ) ) ;
#181949=EDGE_CURVE ( 'NONE', #89587, #10420, #34274, .T. ) ;
#182035=EDGE_CURVE ( 'NONE', #7157, #98258, #176680, .T. ) ;
#182212=EDGE_CURVE ( 'NONE', #165860, #138761, #118518, .T. ) ;
#182406=LINE ( 'NONE', #55063, #20390 ) ;
#182418=VECTOR ( 'NONE', #95371, 999.9999999999997726 ) ;
#182607=DIRECTION ( 'NONE',  ( 1.000000000000000000, 0.000000000000000000, 0.000000000000000000 ) ) ;
#182855=EDGE_CURVE ( 'NONE', #26587, #183244, #74575, .T. ) ;
#183244=VERTEX_POINT ( 'NONE', #167582 ) ;
#183319=TOROIDAL_SURFACE ( 'NONE', #57338, 4.000000000000000000, 0.2500000000000000000 ) ;
#183853=ADVANCED_FACE ( 'NONE', ( #126038, #93703 ), #78526, .T. ) ;
#184086=VERTEX_POINT ( 'NONE', #127014 ) ;
#184907=CARTESIAN_POINT ( 'NONE',  ( 12.99999999999999822, 2.789133085058097101E-16, -2.055000000000000160 ) ) ;
#184981=ORIENTED_EDGE ( 'NONE', *, *, #136550, .F. ) ;
#184990=FACE_OUTER_BOUND ( 'NONE', #15966, .T. ) ;
#185376=AXIS2_PLACEMENT_3D ( 'NONE', #150571, #56559, #152533 ) ;
#185879=AXIS2_PLACEMENT_3D ( 'NONE', #109675, #124846, #32844 ) ;
#186141=CARTESIAN_POINT ( 'NONE',  ( 2.500000000000000000, -2.357898499370432610, 3.252606517456513302E-15 ) ) ;
#186181=FACE_OUTER_BOUND ( 'NONE', #60520, .T. ) ;
#186342=ORIENTED_EDGE ( 'NONE', *, *, #86135, .T. ) ;
#186780=DIRECTION ( 'NONE',  ( 0.000000000000000000, 0.000000000000000000, 1.000000000000000000 ) ) ;
#186801=CIRCLE ( 'NONE', #157759, 2.500000000000000444 ) ;
#186961=EDGE_CURVE ( 'NONE', #139778, #89587, #42779, .T. ) ;
#187194=AXIS2_PLACEMENT_3D ( 'NONE', #56664, #118337, #30288 ) ;
#187266=FACE_OUTER_BOUND ( 'NONE', #77849, .T. ) ;
#187299=VECTOR ( 'NONE', #137629, 1000.000000000000000 ) ;
#187359=EDGE_CURVE ( 'NONE', #168893, #92733, #173055, .T. ) ;
#187423=DIRECTION ( 'NONE',  ( 0.000000000000000000, -1.287488025362403787E-15, -1.000000000000000000 ) ) ;
#187529=EDGE_LOOP ( 'NONE', ( #23578, #88422, #118854, #125154, #62443 ) ) ;
#187749=CARTESIAN_POINT ( 'NONE',  ( 2.500000000000000000, 2.357898499370431722, -2.818925648462311528E-15 ) ) ;
#187769=CARTESIAN_POINT ( 'NONE',  ( 5.199999999999996625, 0.000000000000000000, 0.000000000000000000 ) ) ;
#187988=DIRECTION ( 'NONE',  ( -0.7071067811865312525, 8.659560562355131306E-17, -0.7071067811865637820 ) ) ;
#188401=CARTESIAN_POINT ( 'NONE',  ( 2.500000000000000000, 1.178949249685212974, -2.042000000000001148 ) ) ;
#188509=EDGE_CURVE ( 'NONE', #168893, #184086, #117115, .T. ) ;
#189000=DIRECTION ( 'NONE',  ( 0.000000000000000000, 0.000000000000000000, 1.000000000000000000 ) ) ;
#189119=CONICAL_SURFACE ( 'NONE', #101937, 2.041999999999999815, 1.047197551196591858 ) ;
#189524=PRODUCT_DEFINITION ( 'UNKNOWN', '', #143706, #5884 ) ;
#190022=FACE_BOUND ( 'NONE', #6226, .T. ) ;
#190263=ORIENTED_EDGE ( 'NONE', *, *, #37032, .F. ) ;
#190360=EDGE_CURVE ( 'NONE', #41053, #165860, #139960, .T. ) ;
#190368=EDGE_CURVE ( 'NONE', #67444, #167085, #96708, .T. ) ;
#190608=ADVANCED_FACE ( 'NONE', ( #140236 ), #156411, .T. ) ;
#190620=ORIENTED_EDGE ( 'NONE', *, *, #151672, .F. ) ;
#191619=PLANE ( 'NONE',  #44177 ) ;
#191976=CARTESIAN_POINT ( 'NONE',  ( 2.500000000000000000, 3.004629197474319246E-15, 2.042000000000000259 ) ) ;
#192000=CARTESIAN_POINT ( 'NONE',  ( 2.500000000000000000, 1.768423874527823791, 1.020999999999998575 ) ) ;
#192245=CARTESIAN_POINT ( 'NONE',  ( 0.2500000000000002220, 4.898587196589412829E-16, -4.000000000000000000 ) ) ;
#192455=CARTESIAN_POINT ( 'NONE',  ( 0.000000000000000000, 1.178949249685212974, -2.042000000000001148 ) ) ;
#192822=VECTOR ( 'NONE', #142538, 1000.000000000000000 ) ;
#192917=LINE ( 'NONE', #115067, #117865 ) ;
#193011=CARTESIAN_POINT ( 'NONE',  ( 2.500000000000000000, 2.357898499370431722, -2.818925648462311528E-15 ) ) ;
#193193=EDGE_LOOP ( 'NONE', ( #136274, #167611, #130994, #93303 ) ) ;
#193223=DIRECTION ( 'NONE',  ( -1.000000000000000000, -0.000000000000000000, -0.000000000000000000 ) ) ;
#193234=DIRECTION ( 'NONE',  ( 1.000000000000000000, 0.000000000000000000, 0.000000000000000000 ) ) ;
#193525=VERTEX_POINT ( 'NONE', #5939 ) ;
#193713=CARTESIAN_POINT ( 'NONE',  ( 5.199999999999996625, 3.061616997868383634E-16, -2.500000000000000444 ) ) ;
#193979=ORIENTED_EDGE ( 'NONE', *, *, #23510, .T. ) ;
#194022=DIRECTION ( 'NONE',  ( 0.000000000000000000, -0.4999999999999993894, 0.8660254037844389297 ) ) ;
#194055=ORIENTED_EDGE ( 'NONE', *, *, #165915, .F. ) ;
#195238=PLANE ( 'NONE',  #166413 ) ;
#195290=ORIENTED_EDGE ( 'NONE', *, *, #50044, .T. ) ;
#196055=( NAMED_UNIT ( * ) SI_UNIT ( $, .STERADIAN. ) SOLID_ANGLE_UNIT ( ) );
#196074=ORIENTED_EDGE ( 'NONE', *, *, #151672, .T. ) ;
#196093=DIRECTION ( 'NONE',  ( 0.000000000000000000, 0.000000000000000000, 1.000000000000000000 ) ) ;
#196719=CYLINDRICAL_SURFACE ( 'NONE', #51827, 4.250000000000000000 ) ;
#197208=CARTESIAN_POINT ( 'NONE',  ( 2.500000000000000000, 1.178949249685217193, 2.041999999999998483 ) ) ;
#197229=FACE_OUTER_BOUND ( 'NONE', #2269, .T. ) ;
#197919=EDGE_CURVE ( 'NONE', #16610, #98258, #107774, .T. ) ;
#197951=AXIS2_PLACEMENT_3D ( 'NONE', #114470, #165004, #26498 ) ;
#198087=EDGE_CURVE ( 'NONE', #184086, #139805, #56135, .T. ) ;
#198096=CARTESIAN_POINT ( 'NONE',  ( 12.55500000000001748, 3.061616997868383634E-16, -2.500000000000000444 ) ) ;
#198841=ORIENTED_EDGE ( 'NONE', *, *, #145481, .T. ) ;
#199350=DIRECTION ( 'NONE',  ( 0.000000000000000000, 0.000000000000000000, 1.000000000000000000 ) ) ;
#200151=ORIENTED_EDGE ( 'NONE', *, *, #182855, .F. ) ;
ENDSEC;
END-ISO-10303-21;
